ISO-10303-21;
HEADER;
/* Generated by software containing ST-Developer
 * from STEP Tools, Inc. (www.steptools.com) 
 */

FILE_DESCRIPTION(
/* description */ ('Fatigue rig crank-slider'),
/* implementation_level */ '2;1');

FILE_NAME(
/* name */ 'Bearing bolt reducer (3).step',
/* time_stamp */ '2026-10-28T03:24:50-07:00',
/* author */ (''),
/* organization */ (''),
/* preprocessor_version */ 'ST-DEVELOPER v20.2',
/* originating_system */ 'Autodesk Translation Framework v15.17.0.0',
/* authorisation */ '');

FILE_SCHEMA (('AUTOMOTIVE_DESIGN { 1 0 10303 214 3 1 1 }'));
ENDSEC;

DATA;
#10=MECHANICAL_DESIGN_GEOMETRIC_PRESENTATION_REPRESENTATION('',(#593),#16911);
#493=SHAPE_REPRESENTATION_RELATIONSHIP('SRR','None',#17132,#543);
#543=ADVANCED_BREP_SHAPE_REPRESENTATION('',(#652),#16861);
#593=STYLED_ITEM('',(#17494),#652);
#652=MANIFOLD_SOLID_BREP('Body1',#8884);
#758=FACE_BOUND('',#1875,.T.);
#759=FACE_BOUND('',#1877,.T.);
#933=PLANE('',#9658);
#934=PLANE('',#9659);
#1291=FACE_OUTER_BOUND('',#1872,.T.);
#1292=FACE_OUTER_BOUND('',#1873,.T.);
#1293=FACE_OUTER_BOUND('',#1874,.T.);
#1294=FACE_OUTER_BOUND('',#1876,.T.);
#1872=EDGE_LOOP('',(#6296,#6297,#6298,#6299));
#1873=EDGE_LOOP('',(#6300,#6301,#6302,#6303));
#1874=EDGE_LOOP('',(#6304));
#1875=EDGE_LOOP('',(#6305));
#1876=EDGE_LOOP('',(#6306));
#1877=EDGE_LOOP('',(#6307));
#2534=LINE('',#13695,#3180);
#2535=LINE('',#13701,#3181);
#3180=VECTOR('',#10962,0.425);
#3181=VECTOR('',#10969,0.645);
#3828=CIRCLE('',#9653,0.425);
#3829=CIRCLE('',#9654,0.425);
#3830=CIRCLE('',#9656,0.645);
#3831=CIRCLE('',#9657,0.645);
#4252=VERTEX_POINT('',#13692);
#4253=VERTEX_POINT('',#13694);
#4254=VERTEX_POINT('',#13698);
#4255=VERTEX_POINT('',#13700);
#5046=EDGE_CURVE('',#4252,#4252,#3828,.T.);
#5047=EDGE_CURVE('',#4252,#4253,#2534,.T.);
#5048=EDGE_CURVE('',#4253,#4253,#3829,.T.);
#5049=EDGE_CURVE('',#4254,#4254,#3830,.T.);
#5050=EDGE_CURVE('',#4254,#4255,#2535,.T.);
#5051=EDGE_CURVE('',#4255,#4255,#3831,.T.);
#6296=ORIENTED_EDGE('',*,*,#5046,.F.);
#6297=ORIENTED_EDGE('',*,*,#5047,.T.);
#6298=ORIENTED_EDGE('',*,*,#5048,.T.);
#6299=ORIENTED_EDGE('',*,*,#5047,.F.);
#6300=ORIENTED_EDGE('',*,*,#5049,.F.);
#6301=ORIENTED_EDGE('',*,*,#5050,.T.);
#6302=ORIENTED_EDGE('',*,*,#5051,.T.);
#6303=ORIENTED_EDGE('',*,*,#5050,.F.);
#6304=ORIENTED_EDGE('',*,*,#5049,.T.);
#6305=ORIENTED_EDGE('',*,*,#5046,.T.);
#6306=ORIENTED_EDGE('',*,*,#5051,.F.);
#6307=ORIENTED_EDGE('',*,*,#5048,.F.);
#8234=CYLINDRICAL_SURFACE('',#9652,0.425);
#8235=CYLINDRICAL_SURFACE('',#9655,0.645);
#8429=ADVANCED_FACE('',(#1291),#8234,.F.);
#8430=ADVANCED_FACE('',(#1292),#8235,.T.);
#8431=ADVANCED_FACE('',(#1293,#758),#933,.T.);
#8432=ADVANCED_FACE('',(#1294,#759),#934,.F.);
#8884=CLOSED_SHELL('',(#8429,#8430,#8431,#8432));
#9651=AXIS2_PLACEMENT_3D('',#13690,#10956,#10957);
#9652=AXIS2_PLACEMENT_3D('',#13691,#10958,#10959);
#9653=AXIS2_PLACEMENT_3D('',#13693,#10960,#10961);
#9654=AXIS2_PLACEMENT_3D('',#13696,#10963,#10964);
#9655=AXIS2_PLACEMENT_3D('',#13697,#10965,#10966);
#9656=AXIS2_PLACEMENT_3D('',#13699,#10967,#10968);
#9657=AXIS2_PLACEMENT_3D('',#13702,#10970,#10971);
#9658=AXIS2_PLACEMENT_3D('',#13703,#10972,#10973);
#9659=AXIS2_PLACEMENT_3D('',#13704,#10974,#10975);
#10956=DIRECTION('axis',(0.,0.,1.));
#10957=DIRECTION('refdir',(1.,0.,0.));
#10958=DIRECTION('center_axis',(0.,0.,1.));
#10959=DIRECTION('ref_axis',(1.,0.,0.));
#10960=DIRECTION('center_axis',(0.,0.,-1.));
#10961=DIRECTION('ref_axis',(1.,0.,0.));
#10962=DIRECTION('',(0.,0.,-1.));
#10963=DIRECTION('center_axis',(0.,0.,-1.));
#10964=DIRECTION('ref_axis',(1.,0.,0.));
#10965=DIRECTION('center_axis',(0.,0.,1.));
#10966=DIRECTION('ref_axis',(1.,0.,0.));
#10967=DIRECTION('center_axis',(0.,0.,1.));
#10968=DIRECTION('ref_axis',(1.,0.,0.));
#10969=DIRECTION('',(0.,0.,-1.));
#10970=DIRECTION('center_axis',(0.,0.,1.));
#10971=DIRECTION('ref_axis',(1.,0.,0.));
#10972=DIRECTION('center_axis',(0.,0.,1.));
#10973=DIRECTION('ref_axis',(1.,0.,0.));
#10974=DIRECTION('center_axis',(0.,0.,1.));
#10975=DIRECTION('ref_axis',(1.,0.,0.));
#13690=CARTESIAN_POINT('',(0.,0.,0.));
#13691=CARTESIAN_POINT('Origin',(4.75,-7.,8.67));
#13692=CARTESIAN_POINT('',(4.325,-7.,9.87));
#13693=CARTESIAN_POINT('Origin',(4.75,-7.,9.87));
#13694=CARTESIAN_POINT('',(4.325,-7.,8.67));
#13695=CARTESIAN_POINT('',(4.325,-7.,8.67));
#13696=CARTESIAN_POINT('Origin',(4.75,-7.,8.67));
#13697=CARTESIAN_POINT('Origin',(4.75,-7.,8.67));
#13698=CARTESIAN_POINT('',(4.105,-7.,9.87));
#13699=CARTESIAN_POINT('Origin',(4.75,-7.,9.87));
#13700=CARTESIAN_POINT('',(4.105,-7.,8.67));
#13701=CARTESIAN_POINT('',(4.105,-7.,8.67));
#13702=CARTESIAN_POINT('Origin',(4.75,-7.,8.67));
#13703=CARTESIAN_POINT('Origin',(4.75,-7.,9.87));
#13704=CARTESIAN_POINT('Origin',(4.75,-7.,8.67));
#16802=UNCERTAINTY_MEASURE_WITH_UNIT(LENGTH_MEASURE(0.001),#16912,
'DISTANCE_ACCURACY_VALUE',
'Maximum model space distance between geometric entities at asserted c
onnectivities');
#16852=UNCERTAINTY_MEASURE_WITH_UNIT(LENGTH_MEASURE(0.001),#16912,
'DISTANCE_ACCURACY_VALUE',
'Maximum model space distance between geometric entities at asserted c
onnectivities');
#16861=(
GEOMETRIC_REPRESENTATION_CONTEXT(3)
GLOBAL_UNCERTAINTY_ASSIGNED_CONTEXT((#16802))
GLOBAL_UNIT_ASSIGNED_CONTEXT((#16912,#16914,#16915))
REPRESENTATION_CONTEXT('','3D')
);
#16911=(
GEOMETRIC_REPRESENTATION_CONTEXT(3)
GLOBAL_UNCERTAINTY_ASSIGNED_CONTEXT((#16852))
GLOBAL_UNIT_ASSIGNED_CONTEXT((#16912,#16914,#16915))
REPRESENTATION_CONTEXT('','3D')
);
#16912=(
LENGTH_UNIT()
NAMED_UNIT(*)
SI_UNIT(.CENTI.,.METRE.)
);
#16914=(
NAMED_UNIT(*)
PLANE_ANGLE_UNIT()
SI_UNIT($,.RADIAN.)
);
#16915=(
NAMED_UNIT(*)
SI_UNIT($,.STERADIAN.)
SOLID_ANGLE_UNIT()
);
#16924=SHAPE_DEFINITION_REPRESENTATION(#16982,#17132);
#16982=PRODUCT_DEFINITION_SHAPE('',$,#17191);
#17132=SHAPE_REPRESENTATION('',(#9651),#16861);
#17182=PRODUCT_DEFINITION_CONTEXT('part definition',#17358,'design');
#17191=PRODUCT_DEFINITION('Bearing bolt reducer (3)',
'Bearing bolt reducer (3)',#17249,#17182);
#17249=PRODUCT_DEFINITION_FORMATION('',$,#17368);
#17358=APPLICATION_CONTEXT(
'Core Data for Automotive Mechanical Design Process');
#17359=PRODUCT_CONTEXT('part definition',#17358,'mechanical');
#17368=PRODUCT('Bearing bolt reducer (3)','Bearing bolt reducer (3)',
'Bearing bolt reducer (3)',(#17359));
#17488=COLOUR_RGB('Black',0.12,0.14,0.17);
#17489=FILL_AREA_STYLE_COLOUR('',#17488);
#17490=FILL_AREA_STYLE('',(#17489));
#17491=SURFACE_STYLE_FILL_AREA(#17490);
#17492=SURFACE_SIDE_STYLE('',(#17491));
#17493=SURFACE_STYLE_USAGE(.BOTH.,#17492);
#17494=PRESENTATION_STYLE_ASSIGNMENT((#17493));
ENDSEC;
END-ISO-10303-21;
